ISO-10303-21;
HEADER;
/* Generated by software containing ST-Developer
 * from STEP Tools, Inc. (www.steptools.com) 
 */

FILE_DESCRIPTION(
/* description */ ('Bin tilter linkage'),
/* implementation_level */ '2;1');

FILE_NAME(
/* name */ 'M4 short cap screw (12).step',
/* time_stamp */ '2026-10-28T03:26:24-07:00',
/* author */ (''),
/* organization */ (''),
/* preprocessor_version */ 'ST-DEVELOPER v20.2',
/* originating_system */ 'Autodesk Translation Framework v15.17.0.0',
/* authorisation */ '');

FILE_SCHEMA (('AUTOMOTIVE_DESIGN { 1 0 10303 214 3 1 1 }'));
ENDSEC;

DATA;
#10=MECHANICAL_DESIGN_GEOMETRIC_PRESENTATION_REPRESENTATION('',(#909),#23728);
#697=SHAPE_REPRESENTATION_RELATIONSHIP('SRR','None',#24162,#803);
#803=ADVANCED_BREP_SHAPE_REPRESENTATION('',(#1022),#23662);
#909=STYLED_ITEM('',(#24772),#1022);
#1022=MANIFOLD_SOLID_BREP('Body1',#12440);
#1306=FACE_BOUND('',#3244,.T.);
#1665=PLANE('',#14448);
#1666=PLANE('',#14453);
#1667=PLANE('',#14456);
#2247=FACE_OUTER_BOUND('',#3243,.T.);
#2248=FACE_OUTER_BOUND('',#3245,.T.);
#2249=FACE_OUTER_BOUND('',#3246,.T.);
#2250=FACE_OUTER_BOUND('',#3247,.T.);
#2251=FACE_OUTER_BOUND('',#3248,.T.);
#3243=EDGE_LOOP('',(#9745));
#3244=EDGE_LOOP('',(#9746));
#3245=EDGE_LOOP('',(#9747,#9748,#9749,#9750));
#3246=EDGE_LOOP('',(#9751));
#3247=EDGE_LOOP('',(#9752,#9753,#9754,#9755));
#3248=EDGE_LOOP('',(#9756));
#4171=LINE('',#21303,#4846);
#4172=LINE('',#21307,#4847);
#4846=VECTOR('',#17350,0.35);
#4847=VECTOR('',#17355,0.199999999999999);
#5563=CIRCLE('',#14449,0.35);
#5564=CIRCLE('',#14450,0.199999999999999);
#5565=CIRCLE('',#14452,0.35);
#5566=CIRCLE('',#14455,0.199999999999999);
#6413=VERTEX_POINT('',#21296);
#6414=VERTEX_POINT('',#21298);
#6415=VERTEX_POINT('',#21301);
#6416=VERTEX_POINT('',#21306);
#7612=EDGE_CURVE('',#6413,#6413,#5563,.T.);
#7613=EDGE_CURVE('',#6414,#6414,#5564,.T.);
#7614=EDGE_CURVE('',#6415,#6415,#5565,.T.);
#7615=EDGE_CURVE('',#6415,#6413,#4171,.T.);
#7616=EDGE_CURVE('',#6414,#6416,#4172,.T.);
#7617=EDGE_CURVE('',#6416,#6416,#5566,.T.);
#9745=ORIENTED_EDGE('',*,*,#7612,.F.);
#9746=ORIENTED_EDGE('',*,*,#7613,.T.);
#9747=ORIENTED_EDGE('',*,*,#7614,.F.);
#9748=ORIENTED_EDGE('',*,*,#7615,.T.);
#9749=ORIENTED_EDGE('',*,*,#7612,.T.);
#9750=ORIENTED_EDGE('',*,*,#7615,.F.);
#9751=ORIENTED_EDGE('',*,*,#7614,.T.);
#9752=ORIENTED_EDGE('',*,*,#7613,.F.);
#9753=ORIENTED_EDGE('',*,*,#7616,.T.);
#9754=ORIENTED_EDGE('',*,*,#7617,.T.);
#9755=ORIENTED_EDGE('',*,*,#7616,.F.);
#9756=ORIENTED_EDGE('',*,*,#7617,.F.);
#11447=CYLINDRICAL_SURFACE('',#14451,0.35);
#11448=CYLINDRICAL_SURFACE('',#14454,0.199999999999999);
#11972=ADVANCED_FACE('',(#2247,#1306),#1665,.F.);
#11973=ADVANCED_FACE('',(#2248),#11447,.T.);
#11974=ADVANCED_FACE('',(#2249),#1666,.T.);
#11975=ADVANCED_FACE('',(#2250),#11448,.T.);
#11976=ADVANCED_FACE('',(#2251),#1667,.F.);
#12440=CLOSED_SHELL('',(#11972,#11973,#11974,#11975,#11976));
#14447=AXIS2_PLACEMENT_3D('',#21294,#17338,#17339);
#14448=AXIS2_PLACEMENT_3D('',#21295,#17340,#17341);
#14449=AXIS2_PLACEMENT_3D('',#21297,#17342,#17343);
#14450=AXIS2_PLACEMENT_3D('',#21299,#17344,#17345);
#14451=AXIS2_PLACEMENT_3D('',#21300,#17346,#17347);
#14452=AXIS2_PLACEMENT_3D('',#21302,#17348,#17349);
#14453=AXIS2_PLACEMENT_3D('',#21304,#17351,#17352);
#14454=AXIS2_PLACEMENT_3D('',#21305,#17353,#17354);
#14455=AXIS2_PLACEMENT_3D('',#21308,#17356,#17357);
#14456=AXIS2_PLACEMENT_3D('',#21309,#17358,#17359);
#17338=DIRECTION('axis',(0.,0.,1.));
#17339=DIRECTION('refdir',(1.,0.,0.));
#17340=DIRECTION('center_axis',(0.,1.,0.));
#17341=DIRECTION('ref_axis',(1.,0.,0.));
#17342=DIRECTION('center_axis',(0.,1.,0.));
#17343=DIRECTION('ref_axis',(1.,0.,0.));
#17344=DIRECTION('center_axis',(0.,1.,0.));
#17345=DIRECTION('ref_axis',(1.,0.,0.));
#17346=DIRECTION('center_axis',(0.,1.,0.));
#17347=DIRECTION('ref_axis',(1.,0.,0.));
#17348=DIRECTION('center_axis',(0.,1.,0.));
#17349=DIRECTION('ref_axis',(1.,0.,0.));
#17350=DIRECTION('',(0.,-1.,0.));
#17351=DIRECTION('center_axis',(0.,1.,0.));
#17352=DIRECTION('ref_axis',(1.,0.,0.));
#17353=DIRECTION('center_axis',(0.,1.,0.));
#17354=DIRECTION('ref_axis',(1.,0.,0.));
#17355=DIRECTION('',(0.,-1.,0.));
#17356=DIRECTION('center_axis',(0.,1.,0.));
#17357=DIRECTION('ref_axis',(1.,0.,0.));
#17358=DIRECTION('center_axis',(0.,1.,0.));
#17359=DIRECTION('ref_axis',(1.,0.,0.));
#21294=CARTESIAN_POINT('',(0.,0.,0.));
#21295=CARTESIAN_POINT('Origin',(10.7050737530542,0.8,19.7283489784518));
#21296=CARTESIAN_POINT('',(10.3550737530542,0.8,19.7283489784518));
#21297=CARTESIAN_POINT('Origin',(10.7050737530542,0.8,19.7283489784518));
#21298=CARTESIAN_POINT('',(10.5050737530542,0.8,19.7283489784518));
#21299=CARTESIAN_POINT('Origin',(10.7050737530542,0.8,19.7283489784518));
#21300=CARTESIAN_POINT('Origin',(10.7050737530542,0.8,19.7283489784518));
#21301=CARTESIAN_POINT('',(10.3550737530542,1.2,19.7283489784518));
#21302=CARTESIAN_POINT('Origin',(10.7050737530542,1.2,19.7283489784518));
#21303=CARTESIAN_POINT('',(10.3550737530542,0.8,19.7283489784518));
#21304=CARTESIAN_POINT('Origin',(10.7050737530542,1.2,19.7283489784518));
#21305=CARTESIAN_POINT('Origin',(10.7050737530542,0.1,19.7283489784518));
#21306=CARTESIAN_POINT('',(10.5050737530542,0.1,19.7283489784518));
#21307=CARTESIAN_POINT('',(10.5050737530542,0.1,19.7283489784518));
#21308=CARTESIAN_POINT('Origin',(10.7050737530542,0.1,19.7283489784518));
#21309=CARTESIAN_POINT('Origin',(10.7050737530542,0.1,19.7283489784518));
#23545=UNCERTAINTY_MEASURE_WITH_UNIT(LENGTH_MEASURE(0.001),#23729,
'DISTANCE_ACCURACY_VALUE',
'Maximum model space distance between geometric entities at asserted c
onnectivities');
#23611=UNCERTAINTY_MEASURE_WITH_UNIT(LENGTH_MEASURE(0.001),#23729,
'DISTANCE_ACCURACY_VALUE',
'Maximum model space distance between geometric entities at asserted c
onnectivities');
#23662=(
GEOMETRIC_REPRESENTATION_CONTEXT(3)
GLOBAL_UNCERTAINTY_ASSIGNED_CONTEXT((#23545))
GLOBAL_UNIT_ASSIGNED_CONTEXT((#23729,#23731,#23732))
REPRESENTATION_CONTEXT('','3D')
);
#23728=(
GEOMETRIC_REPRESENTATION_CONTEXT(3)
GLOBAL_UNCERTAINTY_ASSIGNED_CONTEXT((#23611))
GLOBAL_UNIT_ASSIGNED_CONTEXT((#23729,#23731,#23732))
REPRESENTATION_CONTEXT('','3D')
);
#23729=(
LENGTH_UNIT()
NAMED_UNIT(*)
SI_UNIT(.CENTI.,.METRE.)
);
#23731=(
NAMED_UNIT(*)
PLANE_ANGLE_UNIT()
SI_UNIT($,.RADIAN.)
);
#23732=(
NAMED_UNIT(*)
SI_UNIT($,.STERADIAN.)
SOLID_ANGLE_UNIT()
);
#23783=SHAPE_DEFINITION_REPRESENTATION(#23899,#24162);
#23899=PRODUCT_DEFINITION_SHAPE('',$,#24279);
#24162=SHAPE_REPRESENTATION('',(#14447),#23662);
#24228=PRODUCT_DEFINITION_CONTEXT('part definition',#24578,'design');
#24279=PRODUCT_DEFINITION('M4 short cap screw (12)',
'M4 short cap screw (12)',#24395,#24228);
#24395=PRODUCT_DEFINITION_FORMATION('',$,#24630);
#24578=APPLICATION_CONTEXT(
'Core Data for Automotive Mechanical Design Process');
#24579=PRODUCT_CONTEXT('part definition',#24578,'mechanical');
#24630=PRODUCT('M4 short cap screw (12)','M4 short cap screw (12)',
'M4 short cap screw (12)',(#24579));
#24766=COLOUR_RGB('Black',0.12,0.14,0.17);
#24767=FILL_AREA_STYLE_COLOUR('',#24766);
#24768=FILL_AREA_STYLE('',(#24767));
#24769=SURFACE_STYLE_FILL_AREA(#24768);
#24770=SURFACE_SIDE_STYLE('',(#24769));
#24771=SURFACE_STYLE_USAGE(.BOTH.,#24770);
#24772=PRESENTATION_STYLE_ASSIGNMENT((#24771));
ENDSEC;
END-ISO-10303-21;
